ISO-10303-21;
HEADER;
/* Generated by software containing ST-Developer
 * from STEP Tools, Inc. (www.steptools.com) 
 */

FILE_DESCRIPTION(
/* description */ ('Twin-shaft manual slide'),
/* implementation_level */ '2;1');

FILE_NAME(
/* name */ 'M5x14 Cap Screw.step',
/* time_stamp */ '2026-10-27T18:38:08-07:00',
/* author */ (''),
/* organization */ (''),
/* preprocessor_version */ 'ST-DEVELOPER v20.2',
/* originating_system */ 'Autodesk Translation Framework v15.17.0.0',
/* authorisation */ '');

FILE_SCHEMA (('AUTOMOTIVE_DESIGN { 1 0 10303 214 3 1 1 }'));
ENDSEC;

DATA;
#10=MECHANICAL_DESIGN_GEOMETRIC_PRESENTATION_REPRESENTATION('',(#279),#6463);
#219=ORIENTED_CLOSED_SHELL('',*,#3641,.F.);
#223=BREP_WITH_VOIDS('Body1',#3642,(#219));
#229=CONICAL_SURFACE('',#3941,0.4,0.785398163397448);
#230=CONICAL_SURFACE('',#3945,0.41,0.785398163397448);
#231=CONICAL_SURFACE('',#3949,0.26,0.463647609000806);
#247=SHAPE_REPRESENTATION_RELATIONSHIP('SRR','None',#6565,#263);
#263=ADVANCED_BREP_SHAPE_REPRESENTATION('',(#223),#6448);
#279=STYLED_ITEM('',(#6747),#223);
#338=FACE_BOUND('',#827,.T.);
#425=PLANE('',#3929);
#426=PLANE('',#3930);
#427=PLANE('',#3931);
#428=PLANE('',#3932);
#429=PLANE('',#3933);
#430=PLANE('',#3934);
#431=PLANE('',#3935);
#432=PLANE('',#3936);
#433=PLANE('',#3937);
#434=PLANE('',#3939);
#435=PLANE('',#3947);
#572=FACE_OUTER_BOUND('',#813,.T.);
#573=FACE_OUTER_BOUND('',#814,.T.);
#574=FACE_OUTER_BOUND('',#815,.T.);
#575=FACE_OUTER_BOUND('',#816,.T.);
#576=FACE_OUTER_BOUND('',#817,.T.);
#577=FACE_OUTER_BOUND('',#818,.T.);
#578=FACE_OUTER_BOUND('',#819,.T.);
#579=FACE_OUTER_BOUND('',#820,.T.);
#580=FACE_OUTER_BOUND('',#821,.T.);
#581=FACE_OUTER_BOUND('',#822,.T.);
#582=FACE_OUTER_BOUND('',#823,.T.);
#583=FACE_OUTER_BOUND('',#824,.T.);
#584=FACE_OUTER_BOUND('',#825,.T.);
#585=FACE_OUTER_BOUND('',#826,.T.);
#586=FACE_OUTER_BOUND('',#828,.T.);
#587=FACE_OUTER_BOUND('',#829,.T.);
#813=EDGE_LOOP('',(#2724,#2725,#2726,#2727));
#814=EDGE_LOOP('',(#2728,#2729,#2730,#2731));
#815=EDGE_LOOP('',(#2732,#2733,#2734,#2735));
#816=EDGE_LOOP('',(#2736,#2737,#2738,#2739));
#817=EDGE_LOOP('',(#2740,#2741,#2742,#2743));
#818=EDGE_LOOP('',(#2744,#2745,#2746,#2747));
#819=EDGE_LOOP('',(#2748,#2749,#2750,#2751,#2752,#2753));
#820=EDGE_LOOP('',(#2754,#2755,#2756,#2757,#2758,#2759));
#821=EDGE_LOOP('',(#2760));
#822=EDGE_LOOP('',(#2761));
#823=EDGE_LOOP('',(#2762,#2763,#2764,#2765));
#824=EDGE_LOOP('',(#2766,#2767,#2768,#2769));
#825=EDGE_LOOP('',(#2770,#2771,#2772,#2773));
#826=EDGE_LOOP('',(#2774));
#827=EDGE_LOOP('',(#2775));
#828=EDGE_LOOP('',(#2776,#2777,#2778,#2779));
#829=EDGE_LOOP('',(#2780,#2781,#2782,#2783));
#1113=LINE('',#5668,#1399);
#1114=LINE('',#5670,#1400);
#1115=LINE('',#5672,#1401);
#1116=LINE('',#5673,#1402);
#1117=LINE('',#5676,#1403);
#1118=LINE('',#5678,#1404);
#1119=LINE('',#5679,#1405);
#1120=LINE('',#5682,#1406);
#1121=LINE('',#5684,#1407);
#1122=LINE('',#5685,#1408);
#1123=LINE('',#5688,#1409);
#1124=LINE('',#5690,#1410);
#1125=LINE('',#5691,#1411);
#1126=LINE('',#5694,#1412);
#1127=LINE('',#5696,#1413);
#1128=LINE('',#5697,#1414);
#1129=LINE('',#5699,#1415);
#1130=LINE('',#5700,#1416);
#1131=LINE('',#5712,#1417);
#1132=LINE('',#5716,#1418);
#1133=LINE('',#5720,#1419);
#1134=LINE('',#5727,#1420);
#1135=LINE('',#5729,#1421);
#1399=VECTOR('',#4533,1.);
#1400=VECTOR('',#4534,1.);
#1401=VECTOR('',#4535,1.);
#1402=VECTOR('',#4536,1.);
#1403=VECTOR('',#4539,1.);
#1404=VECTOR('',#4540,1.);
#1405=VECTOR('',#4541,1.);
#1406=VECTOR('',#4544,1.);
#1407=VECTOR('',#4545,1.);
#1408=VECTOR('',#4546,1.);
#1409=VECTOR('',#4549,1.);
#1410=VECTOR('',#4550,1.);
#1411=VECTOR('',#4551,1.);
#1412=VECTOR('',#4554,1.);
#1413=VECTOR('',#4555,1.);
#1414=VECTOR('',#4556,1.);
#1415=VECTOR('',#4559,1.);
#1416=VECTOR('',#4560,1.);
#1417=VECTOR('',#4577,0.4);
#1418=VECTOR('',#4582,0.425);
#1419=VECTOR('',#4587,0.41);
#1420=VECTOR('',#4596,0.26);
#1421=VECTOR('',#4599,0.25);
#1651=CIRCLE('',#3938,0.24505);
#1652=CIRCLE('',#3940,0.375);
#1653=CIRCLE('',#3942,0.425);
#1654=CIRCLE('',#3944,0.425);
#1655=CIRCLE('',#3946,0.395);
#1656=CIRCLE('',#3948,0.27);
#1657=CIRCLE('',#3950,0.24505);
#1840=VERTEX_POINT('',#5666);
#1841=VERTEX_POINT('',#5667);
#1842=VERTEX_POINT('',#5669);
#1843=VERTEX_POINT('',#5671);
#1844=VERTEX_POINT('',#5675);
#1845=VERTEX_POINT('',#5677);
#1846=VERTEX_POINT('',#5681);
#1847=VERTEX_POINT('',#5683);
#1848=VERTEX_POINT('',#5687);
#1849=VERTEX_POINT('',#5689);
#1850=VERTEX_POINT('',#5693);
#1851=VERTEX_POINT('',#5695);
#1852=VERTEX_POINT('',#5704);
#1853=VERTEX_POINT('',#5707);
#1854=VERTEX_POINT('',#5710);
#1855=VERTEX_POINT('',#5714);
#1856=VERTEX_POINT('',#5718);
#1857=VERTEX_POINT('',#5722);
#1858=VERTEX_POINT('',#5725);
#2167=EDGE_CURVE('',#1840,#1841,#1113,.T.);
#2168=EDGE_CURVE('',#1841,#1842,#1114,.T.);
#2169=EDGE_CURVE('',#1842,#1843,#1115,.T.);
#2170=EDGE_CURVE('',#1840,#1843,#1116,.T.);
#2171=EDGE_CURVE('',#1841,#1844,#1117,.T.);
#2172=EDGE_CURVE('',#1844,#1845,#1118,.T.);
#2173=EDGE_CURVE('',#1845,#1842,#1119,.T.);
#2174=EDGE_CURVE('',#1844,#1846,#1120,.T.);
#2175=EDGE_CURVE('',#1846,#1847,#1121,.T.);
#2176=EDGE_CURVE('',#1847,#1845,#1122,.T.);
#2177=EDGE_CURVE('',#1846,#1848,#1123,.T.);
#2178=EDGE_CURVE('',#1848,#1849,#1124,.T.);
#2179=EDGE_CURVE('',#1849,#1847,#1125,.T.);
#2180=EDGE_CURVE('',#1848,#1850,#1126,.T.);
#2181=EDGE_CURVE('',#1850,#1851,#1127,.T.);
#2182=EDGE_CURVE('',#1851,#1849,#1128,.T.);
#2183=EDGE_CURVE('',#1850,#1840,#1129,.T.);
#2184=EDGE_CURVE('',#1843,#1851,#1130,.T.);
#2185=EDGE_CURVE('',#1852,#1852,#1651,.T.);
#2186=EDGE_CURVE('',#1853,#1853,#1652,.T.);
#2187=EDGE_CURVE('',#1854,#1854,#1653,.T.);
#2188=EDGE_CURVE('',#1854,#1853,#1131,.T.);
#2189=EDGE_CURVE('',#1855,#1855,#1654,.T.);
#2190=EDGE_CURVE('',#1855,#1854,#1132,.T.);
#2191=EDGE_CURVE('',#1856,#1856,#1655,.T.);
#2192=EDGE_CURVE('',#1856,#1855,#1133,.T.);
#2193=EDGE_CURVE('',#1857,#1857,#1656,.T.);
#2194=EDGE_CURVE('',#1858,#1858,#1657,.F.);
#2195=EDGE_CURVE('',#1858,#1857,#1134,.T.);
#2196=EDGE_CURVE('',#1852,#1858,#1135,.T.);
#2724=ORIENTED_EDGE('',*,*,#2167,.T.);
#2725=ORIENTED_EDGE('',*,*,#2168,.T.);
#2726=ORIENTED_EDGE('',*,*,#2169,.T.);
#2727=ORIENTED_EDGE('',*,*,#2170,.F.);
#2728=ORIENTED_EDGE('',*,*,#2171,.T.);
#2729=ORIENTED_EDGE('',*,*,#2172,.T.);
#2730=ORIENTED_EDGE('',*,*,#2173,.T.);
#2731=ORIENTED_EDGE('',*,*,#2168,.F.);
#2732=ORIENTED_EDGE('',*,*,#2174,.T.);
#2733=ORIENTED_EDGE('',*,*,#2175,.T.);
#2734=ORIENTED_EDGE('',*,*,#2176,.T.);
#2735=ORIENTED_EDGE('',*,*,#2172,.F.);
#2736=ORIENTED_EDGE('',*,*,#2177,.T.);
#2737=ORIENTED_EDGE('',*,*,#2178,.T.);
#2738=ORIENTED_EDGE('',*,*,#2179,.T.);
#2739=ORIENTED_EDGE('',*,*,#2175,.F.);
#2740=ORIENTED_EDGE('',*,*,#2180,.T.);
#2741=ORIENTED_EDGE('',*,*,#2181,.T.);
#2742=ORIENTED_EDGE('',*,*,#2182,.T.);
#2743=ORIENTED_EDGE('',*,*,#2178,.F.);
#2744=ORIENTED_EDGE('',*,*,#2183,.T.);
#2745=ORIENTED_EDGE('',*,*,#2170,.T.);
#2746=ORIENTED_EDGE('',*,*,#2184,.T.);
#2747=ORIENTED_EDGE('',*,*,#2181,.F.);
#2748=ORIENTED_EDGE('',*,*,#2183,.F.);
#2749=ORIENTED_EDGE('',*,*,#2180,.F.);
#2750=ORIENTED_EDGE('',*,*,#2177,.F.);
#2751=ORIENTED_EDGE('',*,*,#2174,.F.);
#2752=ORIENTED_EDGE('',*,*,#2171,.F.);
#2753=ORIENTED_EDGE('',*,*,#2167,.F.);
#2754=ORIENTED_EDGE('',*,*,#2184,.F.);
#2755=ORIENTED_EDGE('',*,*,#2169,.F.);
#2756=ORIENTED_EDGE('',*,*,#2173,.F.);
#2757=ORIENTED_EDGE('',*,*,#2176,.F.);
#2758=ORIENTED_EDGE('',*,*,#2179,.F.);
#2759=ORIENTED_EDGE('',*,*,#2182,.F.);
#2760=ORIENTED_EDGE('',*,*,#2185,.F.);
#2761=ORIENTED_EDGE('',*,*,#2186,.F.);
#2762=ORIENTED_EDGE('',*,*,#2187,.F.);
#2763=ORIENTED_EDGE('',*,*,#2188,.T.);
#2764=ORIENTED_EDGE('',*,*,#2186,.T.);
#2765=ORIENTED_EDGE('',*,*,#2188,.F.);
#2766=ORIENTED_EDGE('',*,*,#2189,.F.);
#2767=ORIENTED_EDGE('',*,*,#2190,.T.);
#2768=ORIENTED_EDGE('',*,*,#2187,.T.);
#2769=ORIENTED_EDGE('',*,*,#2190,.F.);
#2770=ORIENTED_EDGE('',*,*,#2191,.F.);
#2771=ORIENTED_EDGE('',*,*,#2192,.T.);
#2772=ORIENTED_EDGE('',*,*,#2189,.T.);
#2773=ORIENTED_EDGE('',*,*,#2192,.F.);
#2774=ORIENTED_EDGE('',*,*,#2191,.T.);
#2775=ORIENTED_EDGE('',*,*,#2193,.F.);
#2776=ORIENTED_EDGE('',*,*,#2194,.F.);
#2777=ORIENTED_EDGE('',*,*,#2195,.T.);
#2778=ORIENTED_EDGE('',*,*,#2193,.T.);
#2779=ORIENTED_EDGE('',*,*,#2195,.F.);
#2780=ORIENTED_EDGE('',*,*,#2185,.T.);
#2781=ORIENTED_EDGE('',*,*,#2196,.T.);
#2782=ORIENTED_EDGE('',*,*,#2194,.T.);
#2783=ORIENTED_EDGE('',*,*,#2196,.F.);
#3386=CYLINDRICAL_SURFACE('',#3943,0.425);
#3387=CYLINDRICAL_SURFACE('',#3951,0.24505);
#3477=ADVANCED_FACE('',(#572),#425,.F.);
#3478=ADVANCED_FACE('',(#573),#426,.F.);
#3479=ADVANCED_FACE('',(#574),#427,.F.);
#3480=ADVANCED_FACE('',(#575),#428,.F.);
#3481=ADVANCED_FACE('',(#576),#429,.F.);
#3482=ADVANCED_FACE('',(#577),#430,.F.);
#3483=ADVANCED_FACE('',(#578),#431,.F.);
#3484=ADVANCED_FACE('',(#579),#432,.F.);
#3485=ADVANCED_FACE('',(#580),#433,.F.);
#3486=ADVANCED_FACE('',(#581),#434,.T.);
#3487=ADVANCED_FACE('',(#582),#229,.T.);
#3488=ADVANCED_FACE('',(#583),#3386,.T.);
#3489=ADVANCED_FACE('',(#584),#230,.T.);
#3490=ADVANCED_FACE('',(#585,#338),#435,.T.);
#3491=ADVANCED_FACE('',(#586),#231,.T.);
#3492=ADVANCED_FACE('',(#587),#3387,.T.);
#3641=CLOSED_SHELL('',(#3477,#3478,#3479,#3480,#3481,#3482,#3483,#3484));
#3642=CLOSED_SHELL('',(#3485,#3486,#3487,#3488,#3489,#3490,#3491,#3492));
#3928=AXIS2_PLACEMENT_3D('',#5664,#4529,#4530);
#3929=AXIS2_PLACEMENT_3D('',#5665,#4531,#4532);
#3930=AXIS2_PLACEMENT_3D('',#5674,#4537,#4538);
#3931=AXIS2_PLACEMENT_3D('',#5680,#4542,#4543);
#3932=AXIS2_PLACEMENT_3D('',#5686,#4547,#4548);
#3933=AXIS2_PLACEMENT_3D('',#5692,#4552,#4553);
#3934=AXIS2_PLACEMENT_3D('',#5698,#4557,#4558);
#3935=AXIS2_PLACEMENT_3D('',#5701,#4561,#4562);
#3936=AXIS2_PLACEMENT_3D('',#5702,#4563,#4564);
#3937=AXIS2_PLACEMENT_3D('',#5703,#4565,#4566);
#3938=AXIS2_PLACEMENT_3D('',#5705,#4567,#4568);
#3939=AXIS2_PLACEMENT_3D('',#5706,#4569,#4570);
#3940=AXIS2_PLACEMENT_3D('',#5708,#4571,#4572);
#3941=AXIS2_PLACEMENT_3D('',#5709,#4573,#4574);
#3942=AXIS2_PLACEMENT_3D('',#5711,#4575,#4576);
#3943=AXIS2_PLACEMENT_3D('',#5713,#4578,#4579);
#3944=AXIS2_PLACEMENT_3D('',#5715,#4580,#4581);
#3945=AXIS2_PLACEMENT_3D('',#5717,#4583,#4584);
#3946=AXIS2_PLACEMENT_3D('',#5719,#4585,#4586);
#3947=AXIS2_PLACEMENT_3D('',#5721,#4588,#4589);
#3948=AXIS2_PLACEMENT_3D('',#5723,#4590,#4591);
#3949=AXIS2_PLACEMENT_3D('',#5724,#4592,#4593);
#3950=AXIS2_PLACEMENT_3D('',#5726,#4594,#4595);
#3951=AXIS2_PLACEMENT_3D('',#5728,#4597,#4598);
#4529=DIRECTION('axis',(0.,0.,1.));
#4530=DIRECTION('refdir',(1.,0.,0.));
#4531=DIRECTION('center_axis',(0.866025403784439,0.,-0.5));
#4532=DIRECTION('ref_axis',(0.5,0.,0.866025403784439));
#4533=DIRECTION('',(-0.5,0.,-0.866025403784439));
#4534=DIRECTION('',(0.,-1.,0.));
#4535=DIRECTION('',(0.5,0.,0.866025403784439));
#4536=DIRECTION('',(0.,-1.,0.));
#4537=DIRECTION('center_axis',(1.20185167898973E-16,0.,-1.));
#4538=DIRECTION('ref_axis',(1.,0.,1.20185167898973E-16));
#4539=DIRECTION('',(-1.,0.,-1.20185167898973E-16));
#4540=DIRECTION('',(0.,-1.,0.));
#4541=DIRECTION('',(1.,0.,1.20185167898973E-16));
#4542=DIRECTION('center_axis',(-0.866025403784439,0.,-0.5));
#4543=DIRECTION('ref_axis',(0.5,0.,-0.866025403784439));
#4544=DIRECTION('',(-0.5,0.,0.866025403784439));
#4545=DIRECTION('',(0.,-1.,0.));
#4546=DIRECTION('',(0.5,0.,-0.866025403784439));
#4547=DIRECTION('center_axis',(-0.866025403784439,0.,0.5));
#4548=DIRECTION('ref_axis',(-0.5,0.,-0.866025403784439));
#4549=DIRECTION('',(0.5,0.,0.866025403784439));
#4550=DIRECTION('',(0.,-1.,0.));
#4551=DIRECTION('',(-0.5,0.,-0.866025403784439));
#4552=DIRECTION('center_axis',(-2.40370335797945E-16,0.,1.));
#4553=DIRECTION('ref_axis',(-1.,0.,-2.40370335797945E-16));
#4554=DIRECTION('',(1.,0.,2.40370335797945E-16));
#4555=DIRECTION('',(0.,-1.,0.));
#4556=DIRECTION('',(-1.,0.,-2.40370335797945E-16));
#4557=DIRECTION('center_axis',(0.866025403784439,0.,0.5));
#4558=DIRECTION('ref_axis',(-0.5,0.,0.866025403784439));
#4559=DIRECTION('',(0.5,0.,-0.866025403784439));
#4560=DIRECTION('',(-0.5,0.,0.866025403784439));
#4561=DIRECTION('center_axis',(0.,1.,0.));
#4562=DIRECTION('ref_axis',(1.,0.,0.));
#4563=DIRECTION('center_axis',(0.,-1.,0.));
#4564=DIRECTION('ref_axis',(0.,0.,-1.));
#4565=DIRECTION('center_axis',(0.,1.,0.));
#4566=DIRECTION('ref_axis',(1.,0.,0.));
#4567=DIRECTION('center_axis',(0.,1.,0.));
#4568=DIRECTION('ref_axis',(1.,0.,0.));
#4569=DIRECTION('center_axis',(0.,1.,0.));
#4570=DIRECTION('ref_axis',(0.,0.,1.));
#4571=DIRECTION('center_axis',(0.,-1.,0.));
#4572=DIRECTION('ref_axis',(1.,0.,0.));
#4573=DIRECTION('center_axis',(0.,-1.,0.));
#4574=DIRECTION('ref_axis',(1.,0.,0.));
#4575=DIRECTION('center_axis',(0.,-1.,0.));
#4576=DIRECTION('ref_axis',(1.,0.,0.));
#4577=DIRECTION('',(0.707106781186548,0.707106781186547,8.65956056235493E-17));
#4578=DIRECTION('center_axis',(0.,-1.,0.));
#4579=DIRECTION('ref_axis',(1.,0.,0.));
#4580=DIRECTION('center_axis',(0.,-1.,0.));
#4581=DIRECTION('ref_axis',(1.,0.,0.));
#4582=DIRECTION('',(0.,1.,0.));
#4583=DIRECTION('center_axis',(0.,1.,0.));
#4584=DIRECTION('ref_axis',(1.,0.,0.));
#4585=DIRECTION('center_axis',(0.,-1.,0.));
#4586=DIRECTION('ref_axis',(1.,0.,0.));
#4587=DIRECTION('',(-0.707106781186547,0.707106781186548,-8.65956056235493E-17));
#4588=DIRECTION('center_axis',(0.,-1.,0.));
#4589=DIRECTION('ref_axis',(0.,0.,-1.));
#4590=DIRECTION('center_axis',(0.,-1.,0.));
#4591=DIRECTION('ref_axis',(1.,0.,0.));
#4592=DIRECTION('center_axis',(0.,1.,0.));
#4593=DIRECTION('ref_axis',(1.,0.,0.));
#4594=DIRECTION('center_axis',(0.,1.,0.));
#4595=DIRECTION('ref_axis',(1.,0.,0.));
#4596=DIRECTION('',(-0.447213595499958,0.894427190999916,-5.47678698264203E-17));
#4597=DIRECTION('center_axis',(0.,-1.,0.));
#4598=DIRECTION('ref_axis',(1.,0.,0.));
#4599=DIRECTION('',(0.,1.,0.));
#5664=CARTESIAN_POINT('',(0.,0.,0.));
#5665=CARTESIAN_POINT('Origin',(0.115470053837925,-0.5,-0.2));
#5666=CARTESIAN_POINT('',(0.23094010767585,-0.5,0.));
#5667=CARTESIAN_POINT('',(0.115470053837925,-0.5,-0.2));
#5668=CARTESIAN_POINT('',(0.23094010767585,-0.5,0.));
#5669=CARTESIAN_POINT('',(0.115470053837925,-0.8,-0.2));
#5670=CARTESIAN_POINT('',(0.115470053837925,-0.5,-0.2));
#5671=CARTESIAN_POINT('',(0.23094010767585,-0.8,0.));
#5672=CARTESIAN_POINT('',(0.23094010767585,-0.8,0.));
#5673=CARTESIAN_POINT('',(0.23094010767585,-0.5,0.));
#5674=CARTESIAN_POINT('Origin',(-0.115470053837925,-0.5,-0.2));
#5675=CARTESIAN_POINT('',(-0.115470053837925,-0.5,-0.2));
#5676=CARTESIAN_POINT('',(0.115470053837925,-0.5,-0.2));
#5677=CARTESIAN_POINT('',(-0.115470053837925,-0.8,-0.2));
#5678=CARTESIAN_POINT('',(-0.115470053837925,-0.5,-0.2));
#5679=CARTESIAN_POINT('',(0.115470053837925,-0.8,-0.2));
#5680=CARTESIAN_POINT('Origin',(-0.23094010767585,-0.5,-2.77555756156289E-17));
#5681=CARTESIAN_POINT('',(-0.23094010767585,-0.5,-2.82820063659975E-17));
#5682=CARTESIAN_POINT('',(-0.115470053837925,-0.5,-0.2));
#5683=CARTESIAN_POINT('',(-0.23094010767585,-0.8,-2.77555756156289E-17));
#5684=CARTESIAN_POINT('',(-0.23094010767585,-0.5,-2.82820063659975E-17));
#5685=CARTESIAN_POINT('',(-0.115470053837925,-0.8,-0.2));
#5686=CARTESIAN_POINT('Origin',(-0.115470053837925,-0.5,0.2));
#5687=CARTESIAN_POINT('',(-0.115470053837925,-0.5,0.2));
#5688=CARTESIAN_POINT('',(-0.23094010767585,-0.5,-2.82820063659975E-17));
#5689=CARTESIAN_POINT('',(-0.115470053837925,-0.8,0.2));
#5690=CARTESIAN_POINT('',(-0.115470053837925,-0.5,0.2));
#5691=CARTESIAN_POINT('',(-0.23094010767585,-0.8,-2.82820063659975E-17));
#5692=CARTESIAN_POINT('Origin',(0.115470053837925,-0.5,0.2));
#5693=CARTESIAN_POINT('',(0.115470053837925,-0.5,0.2));
#5694=CARTESIAN_POINT('',(-0.115470053837925,-0.5,0.2));
#5695=CARTESIAN_POINT('',(0.115470053837925,-0.8,0.2));
#5696=CARTESIAN_POINT('',(0.115470053837925,-0.5,0.2));
#5697=CARTESIAN_POINT('',(-0.115470053837925,-0.8,0.2));
#5698=CARTESIAN_POINT('Origin',(0.23094010767585,-0.5,0.));
#5699=CARTESIAN_POINT('',(0.115470053837925,-0.5,0.2));
#5700=CARTESIAN_POINT('',(0.115470053837925,-0.8,0.2));
#5701=CARTESIAN_POINT('Origin',(0.,-0.5,0.));
#5702=CARTESIAN_POINT('Origin',(0.,-0.8,0.));
#5703=CARTESIAN_POINT('Origin',(0.,-1.4,0.));
#5704=CARTESIAN_POINT('',(-0.24505,-1.4,3.00099698131059E-17));
#5705=CARTESIAN_POINT('Origin',(0.,-1.4,0.));
#5706=CARTESIAN_POINT('Origin',(0.375,0.5,0.));
#5707=CARTESIAN_POINT('',(-0.375,0.5,-4.59242549680257E-17));
#5708=CARTESIAN_POINT('Origin',(0.,0.5,0.));
#5709=CARTESIAN_POINT('Origin',(0.,0.475,0.));
#5710=CARTESIAN_POINT('',(-0.425,0.45,-5.20474889637625E-17));
#5711=CARTESIAN_POINT('Origin',(0.,0.45,0.));
#5712=CARTESIAN_POINT('',(-0.4,0.475,-4.89858719658941E-17));
#5713=CARTESIAN_POINT('Origin',(0.,0.24,0.));
#5714=CARTESIAN_POINT('',(-0.425,0.0299999999999998,-5.20474889637625E-17));
#5715=CARTESIAN_POINT('Origin',(0.,0.0299999999999998,0.));
#5716=CARTESIAN_POINT('',(-0.425,0.24,-5.20474889637625E-17));
#5717=CARTESIAN_POINT('Origin',(0.,0.0150000000000001,0.));
#5718=CARTESIAN_POINT('',(-0.395,4.85722573273506E-17,-4.83735485663204E-17));
#5719=CARTESIAN_POINT('Origin',(0.,0.,0.));
#5720=CARTESIAN_POINT('',(-0.41,0.0150000000000001,-5.02105187650415E-17));
#5721=CARTESIAN_POINT('Origin',(0.27,0.,0.));
#5722=CARTESIAN_POINT('',(-0.27,0.,-3.30654635769785E-17));
#5723=CARTESIAN_POINT('Origin',(0.,0.,0.));
#5724=CARTESIAN_POINT('Origin',(0.,-0.02,0.));
#5725=CARTESIAN_POINT('',(-0.24505,-0.0498999999999999,3.00099698131059E-17));
#5726=CARTESIAN_POINT('Origin',(0.,-0.0498999999999999,0.));
#5727=CARTESIAN_POINT('',(-0.26,-0.02,-3.18408167778312E-17));
#5728=CARTESIAN_POINT('Origin',(0.,-0.995,0.));
#5729=CARTESIAN_POINT('',(-0.24505,-0.995,-3.00099698131059E-17));
#6427=UNCERTAINTY_MEASURE_WITH_UNIT(LENGTH_MEASURE(0.001),#6464,
'DISTANCE_ACCURACY_VALUE',
'Maximum model space distance between geometric entities at asserted c
onnectivities');
#6442=UNCERTAINTY_MEASURE_WITH_UNIT(LENGTH_MEASURE(0.001),#6464,
'DISTANCE_ACCURACY_VALUE',
'Maximum model space distance between geometric entities at asserted c
onnectivities');
#6448=(
GEOMETRIC_REPRESENTATION_CONTEXT(3)
GLOBAL_UNCERTAINTY_ASSIGNED_CONTEXT((#6427))
GLOBAL_UNIT_ASSIGNED_CONTEXT((#6464,#6466,#6467))
REPRESENTATION_CONTEXT('','3D')
);
#6463=(
GEOMETRIC_REPRESENTATION_CONTEXT(3)
GLOBAL_UNCERTAINTY_ASSIGNED_CONTEXT((#6442))
GLOBAL_UNIT_ASSIGNED_CONTEXT((#6464,#6466,#6467))
REPRESENTATION_CONTEXT('','3D')
);
#6464=(
LENGTH_UNIT()
NAMED_UNIT(*)
SI_UNIT(.CENTI.,.METRE.)
);
#6466=(
NAMED_UNIT(*)
PLANE_ANGLE_UNIT()
SI_UNIT($,.RADIAN.)
);
#6467=(
NAMED_UNIT(*)
SI_UNIT($,.STERADIAN.)
SOLID_ANGLE_UNIT()
);
#6473=SHAPE_DEFINITION_REPRESENTATION(#6493,#6565);
#6493=PRODUCT_DEFINITION_SHAPE('',$,#6586);
#6565=SHAPE_REPRESENTATION('',(#3928),#6448);
#6580=PRODUCT_DEFINITION_CONTEXT('part definition',#6642,'design');
#6586=PRODUCT_DEFINITION('M5x14 Cap Screw','M5x14 Cap Screw',#6606,#6580);
#6606=PRODUCT_DEFINITION_FORMATION('',$,#6649);
#6642=APPLICATION_CONTEXT(
'Core Data for Automotive Mechanical Design Process');
#6643=PRODUCT_CONTEXT('part definition',#6642,'mechanical');
#6649=PRODUCT('M5x14 Cap Screw','M5x14 Cap Screw','M5x14 Cap Screw',(#6643));
#6741=COLOUR_RGB('Black',0.12,0.14,0.17);
#6742=FILL_AREA_STYLE_COLOUR('',#6741);
#6743=FILL_AREA_STYLE('',(#6742));
#6744=SURFACE_STYLE_FILL_AREA(#6743);
#6745=SURFACE_SIDE_STYLE('',(#6744));
#6746=SURFACE_STYLE_USAGE(.BOTH.,#6745);
#6747=PRESENTATION_STYLE_ASSIGNMENT((#6746));
ENDSEC;
END-ISO-10303-21;
